ISO-10303-21;
HEADER;
/* Generated by software containing ST-Developer
 * from STEP Tools, Inc. (www.steptools.com) 
 */

FILE_DESCRIPTION(
/* description */ (''),
/* implementation_level */ '2;1');

FILE_NAME(
/* name */ 'Bearing_04.step',
/* time_stamp */ '2026-10-19T01:30:23+06:00',
/* author */ (''),
/* organization */ (''),
/* preprocessor_version */ 'ST-DEVELOPER v20.2',
/* originating_system */ 'Autodesk Translation Framework v15.15.0.0',
/* authorisation */ '');

FILE_SCHEMA (('AUTOMOTIVE_DESIGN { 1 0 10303 214 3 1 1 }'));
ENDSEC;

DATA;
#10=MECHANICAL_DESIGN_GEOMETRIC_PRESENTATION_REPRESENTATION('',(#89),#10639);
#69=SHAPE_REPRESENTATION_RELATIONSHIP('SRR','None',#10679,#79);
#79=ADVANCED_BREP_SHAPE_REPRESENTATION('',(#99),#10631);
#89=STYLED_ITEM('',(#10790),#99);
#99=MANIFOLD_SOLID_BREP('Bearing_04',#5715);
#211=TOROIDAL_SURFACE('',#6200,4.3,0.3);
#212=TOROIDAL_SURFACE('',#6210,4.7,0.3);
#213=TOROIDAL_SURFACE('',#6217,4.3,0.3);
#214=TOROIDAL_SURFACE('',#6222,4.7,0.3);
#272=FACE_BOUND('',#963,.T.);
#273=FACE_BOUND('',#969,.T.);
#339=PLANE('',#6205);
#340=PLANE('',#6220);
#549=FACE_OUTER_BOUND('',#961,.T.);
#550=FACE_OUTER_BOUND('',#962,.T.);
#551=FACE_OUTER_BOUND('',#964,.T.);
#552=FACE_OUTER_BOUND('',#965,.T.);
#553=FACE_OUTER_BOUND('',#966,.T.);
#554=FACE_OUTER_BOUND('',#967,.T.);
#555=FACE_OUTER_BOUND('',#968,.T.);
#556=FACE_OUTER_BOUND('',#970,.T.);
#961=EDGE_LOOP('',(#4234,#4235,#4236,#4237,#4238));
#962=EDGE_LOOP('',(#4239));
#963=EDGE_LOOP('',(#4240));
#964=EDGE_LOOP('',(#4241,#4242,#4243,#4244,#4245,#4246));
#965=EDGE_LOOP('',(#4247,#4248,#4249,#4250,#4251));
#966=EDGE_LOOP('',(#4252,#4253,#4254,#4255,#4256,#4257));
#967=EDGE_LOOP('',(#4258,#4259,#4260,#4261,#4262));
#968=EDGE_LOOP('',(#4263));
#969=EDGE_LOOP('',(#4264));
#970=EDGE_LOOP('',(#4265,#4266,#4267,#4268,#4269));
#1349=LINE('',#9470,#1679);
#1350=LINE('',#9482,#1680);
#1679=VECTOR('',#7589,4.);
#1680=VECTOR('',#7604,5.);
#2044=CIRCLE('',#6201,4.3);
#2045=CIRCLE('',#6202,0.3);
#2046=CIRCLE('',#6203,4.);
#2047=CIRCLE('',#6204,4.);
#2048=CIRCLE('',#6206,4.7);
#2049=CIRCLE('',#6208,4.);
#2050=CIRCLE('',#6209,4.);
#2051=CIRCLE('',#6211,0.3);
#2052=CIRCLE('',#6212,5.);
#2053=CIRCLE('',#6213,5.);
#2054=CIRCLE('',#6215,5.);
#2055=CIRCLE('',#6216,5.);
#2056=CIRCLE('',#6218,4.3);
#2057=CIRCLE('',#6219,0.3);
#2058=CIRCLE('',#6221,4.7);
#2059=CIRCLE('',#6223,0.3);
#2498=VERTEX_POINT('',#9458);
#2499=VERTEX_POINT('',#9460);
#2500=VERTEX_POINT('',#9462);
#2501=VERTEX_POINT('',#9466);
#2502=VERTEX_POINT('',#9469);
#2503=VERTEX_POINT('',#9471);
#2504=VERTEX_POINT('',#9475);
#2505=VERTEX_POINT('',#9477);
#2506=VERTEX_POINT('',#9481);
#2507=VERTEX_POINT('',#9483);
#2508=VERTEX_POINT('',#9487);
#2509=VERTEX_POINT('',#9491);
#3093=EDGE_CURVE('',#2498,#2498,#2044,.T.);
#3094=EDGE_CURVE('',#2498,#2499,#2045,.T.);
#3095=EDGE_CURVE('',#2499,#2500,#2046,.T.);
#3096=EDGE_CURVE('',#2500,#2499,#2047,.T.);
#3097=EDGE_CURVE('',#2501,#2501,#2048,.T.);
#3098=EDGE_CURVE('',#2500,#2502,#1349,.T.);
#3099=EDGE_CURVE('',#2503,#2502,#2049,.T.);
#3100=EDGE_CURVE('',#2502,#2503,#2050,.T.);
#3101=EDGE_CURVE('',#2501,#2504,#2051,.T.);
#3102=EDGE_CURVE('',#2504,#2505,#2052,.T.);
#3103=EDGE_CURVE('',#2505,#2504,#2053,.T.);
#3104=EDGE_CURVE('',#2505,#2506,#1350,.T.);
#3105=EDGE_CURVE('',#2507,#2506,#2054,.T.);
#3106=EDGE_CURVE('',#2506,#2507,#2055,.T.);
#3107=EDGE_CURVE('',#2508,#2508,#2056,.T.);
#3108=EDGE_CURVE('',#2508,#2503,#2057,.T.);
#3109=EDGE_CURVE('',#2509,#2509,#2058,.T.);
#3110=EDGE_CURVE('',#2509,#2507,#2059,.T.);
#4234=ORIENTED_EDGE('',*,*,#3093,.T.);
#4235=ORIENTED_EDGE('',*,*,#3094,.T.);
#4236=ORIENTED_EDGE('',*,*,#3095,.T.);
#4237=ORIENTED_EDGE('',*,*,#3096,.T.);
#4238=ORIENTED_EDGE('',*,*,#3094,.F.);
#4239=ORIENTED_EDGE('',*,*,#3097,.F.);
#4240=ORIENTED_EDGE('',*,*,#3093,.F.);
#4241=ORIENTED_EDGE('',*,*,#3096,.F.);
#4242=ORIENTED_EDGE('',*,*,#3098,.T.);
#4243=ORIENTED_EDGE('',*,*,#3099,.F.);
#4244=ORIENTED_EDGE('',*,*,#3100,.F.);
#4245=ORIENTED_EDGE('',*,*,#3098,.F.);
#4246=ORIENTED_EDGE('',*,*,#3095,.F.);
#4247=ORIENTED_EDGE('',*,*,#3097,.T.);
#4248=ORIENTED_EDGE('',*,*,#3101,.T.);
#4249=ORIENTED_EDGE('',*,*,#3102,.T.);
#4250=ORIENTED_EDGE('',*,*,#3103,.T.);
#4251=ORIENTED_EDGE('',*,*,#3101,.F.);
#4252=ORIENTED_EDGE('',*,*,#3103,.F.);
#4253=ORIENTED_EDGE('',*,*,#3104,.T.);
#4254=ORIENTED_EDGE('',*,*,#3105,.F.);
#4255=ORIENTED_EDGE('',*,*,#3106,.F.);
#4256=ORIENTED_EDGE('',*,*,#3104,.F.);
#4257=ORIENTED_EDGE('',*,*,#3102,.F.);
#4258=ORIENTED_EDGE('',*,*,#3107,.T.);
#4259=ORIENTED_EDGE('',*,*,#3108,.T.);
#4260=ORIENTED_EDGE('',*,*,#3099,.T.);
#4261=ORIENTED_EDGE('',*,*,#3100,.T.);
#4262=ORIENTED_EDGE('',*,*,#3108,.F.);
#4263=ORIENTED_EDGE('',*,*,#3109,.F.);
#4264=ORIENTED_EDGE('',*,*,#3107,.F.);
#4265=ORIENTED_EDGE('',*,*,#3109,.T.);
#4266=ORIENTED_EDGE('',*,*,#3110,.T.);
#4267=ORIENTED_EDGE('',*,*,#3105,.T.);
#4268=ORIENTED_EDGE('',*,*,#3106,.T.);
#4269=ORIENTED_EDGE('',*,*,#3110,.F.);
#5225=CYLINDRICAL_SURFACE('',#6207,4.);
#5226=CYLINDRICAL_SURFACE('',#6214,5.);
#5492=ADVANCED_FACE('',(#549),#211,.T.);
#5493=ADVANCED_FACE('',(#550,#272),#339,.F.);
#5494=ADVANCED_FACE('',(#551),#5225,.F.);
#5495=ADVANCED_FACE('',(#552),#212,.T.);
#5496=ADVANCED_FACE('',(#553),#5226,.T.);
#5497=ADVANCED_FACE('',(#554),#213,.T.);
#5498=ADVANCED_FACE('',(#555,#273),#340,.T.);
#5499=ADVANCED_FACE('',(#556),#214,.T.);
#5715=CLOSED_SHELL('',(#5492,#5493,#5494,#5495,#5496,#5497,#5498,#5499));
#6199=AXIS2_PLACEMENT_3D('',#9456,#7571,#7572);
#6200=AXIS2_PLACEMENT_3D('',#9457,#7573,#7574);
#6201=AXIS2_PLACEMENT_3D('',#9459,#7575,#7576);
#6202=AXIS2_PLACEMENT_3D('',#9461,#7577,#7578);
#6203=AXIS2_PLACEMENT_3D('',#9463,#7579,#7580);
#6204=AXIS2_PLACEMENT_3D('',#9464,#7581,#7582);
#6205=AXIS2_PLACEMENT_3D('',#9465,#7583,#7584);
#6206=AXIS2_PLACEMENT_3D('',#9467,#7585,#7586);
#6207=AXIS2_PLACEMENT_3D('',#9468,#7587,#7588);
#6208=AXIS2_PLACEMENT_3D('',#9472,#7590,#7591);
#6209=AXIS2_PLACEMENT_3D('',#9473,#7592,#7593);
#6210=AXIS2_PLACEMENT_3D('',#9474,#7594,#7595);
#6211=AXIS2_PLACEMENT_3D('',#9476,#7596,#7597);
#6212=AXIS2_PLACEMENT_3D('',#9478,#7598,#7599);
#6213=AXIS2_PLACEMENT_3D('',#9479,#7600,#7601);
#6214=AXIS2_PLACEMENT_3D('',#9480,#7602,#7603);
#6215=AXIS2_PLACEMENT_3D('',#9484,#7605,#7606);
#6216=AXIS2_PLACEMENT_3D('',#9485,#7607,#7608);
#6217=AXIS2_PLACEMENT_3D('',#9486,#7609,#7610);
#6218=AXIS2_PLACEMENT_3D('',#9488,#7611,#7612);
#6219=AXIS2_PLACEMENT_3D('',#9489,#7613,#7614);
#6220=AXIS2_PLACEMENT_3D('',#9490,#7615,#7616);
#6221=AXIS2_PLACEMENT_3D('',#9492,#7617,#7618);
#6222=AXIS2_PLACEMENT_3D('',#9493,#7619,#7620);
#6223=AXIS2_PLACEMENT_3D('',#9494,#7621,#7622);
#7571=DIRECTION('axis',(0.,0.,1.));
#7572=DIRECTION('refdir',(1.,0.,0.));
#7573=DIRECTION('center_axis',(1.,0.,0.));
#7574=DIRECTION('ref_axis',(0.,0.,1.));
#7575=DIRECTION('center_axis',(-1.,0.,0.));
#7576=DIRECTION('ref_axis',(0.,1.,0.));
#7577=DIRECTION('center_axis',(0.,1.,0.));
#7578=DIRECTION('ref_axis',(0.,0.,-1.));
#7579=DIRECTION('center_axis',(1.,0.,0.));
#7580=DIRECTION('ref_axis',(0.,1.,0.));
#7581=DIRECTION('center_axis',(1.,0.,0.));
#7582=DIRECTION('ref_axis',(0.,1.,0.));
#7583=DIRECTION('center_axis',(1.,0.,0.));
#7584=DIRECTION('ref_axis',(0.,1.,0.));
#7585=DIRECTION('center_axis',(1.,0.,0.));
#7586=DIRECTION('ref_axis',(0.,1.,0.));
#7587=DIRECTION('center_axis',(-1.,0.,0.));
#7588=DIRECTION('ref_axis',(0.,1.,0.));
#7589=DIRECTION('',(1.,0.,0.));
#7590=DIRECTION('center_axis',(-1.,0.,0.));
#7591=DIRECTION('ref_axis',(0.,1.,0.));
#7592=DIRECTION('center_axis',(-1.,0.,0.));
#7593=DIRECTION('ref_axis',(0.,1.,0.));
#7594=DIRECTION('center_axis',(-1.,0.,0.));
#7595=DIRECTION('ref_axis',(0.,0.,-1.));
#7596=DIRECTION('center_axis',(0.,1.,0.));
#7597=DIRECTION('ref_axis',(0.,0.,1.));
#7598=DIRECTION('center_axis',(-1.,0.,0.));
#7599=DIRECTION('ref_axis',(0.,1.,0.));
#7600=DIRECTION('center_axis',(-1.,0.,0.));
#7601=DIRECTION('ref_axis',(0.,1.,0.));
#7602=DIRECTION('center_axis',(-1.,0.,0.));
#7603=DIRECTION('ref_axis',(0.,1.,0.));
#7604=DIRECTION('',(1.,0.,0.));
#7605=DIRECTION('center_axis',(1.,0.,0.));
#7606=DIRECTION('ref_axis',(0.,1.,0.));
#7607=DIRECTION('center_axis',(1.,0.,0.));
#7608=DIRECTION('ref_axis',(0.,1.,0.));
#7609=DIRECTION('center_axis',(-1.,0.,0.));
#7610=DIRECTION('ref_axis',(0.,0.,-1.));
#7611=DIRECTION('center_axis',(1.,0.,0.));
#7612=DIRECTION('ref_axis',(0.,1.,0.));
#7613=DIRECTION('center_axis',(0.,1.,0.));
#7614=DIRECTION('ref_axis',(0.,0.,1.));
#7615=DIRECTION('center_axis',(1.,0.,0.));
#7616=DIRECTION('ref_axis',(0.,1.,0.));
#7617=DIRECTION('center_axis',(-1.,0.,0.));
#7618=DIRECTION('ref_axis',(0.,1.,0.));
#7619=DIRECTION('center_axis',(1.,0.,0.));
#7620=DIRECTION('ref_axis',(0.,0.,1.));
#7621=DIRECTION('center_axis',(0.,1.,0.));
#7622=DIRECTION('ref_axis',(0.,0.,-1.));
#9456=CARTESIAN_POINT('',(0.,0.,0.));
#9457=CARTESIAN_POINT('Origin',(13.3,-21.9999999999999,-1.92966607280848));
#9458=CARTESIAN_POINT('',(13.,-21.9999999999999,-6.22966607280848));
#9459=CARTESIAN_POINT('Origin',(13.,-21.9999999999999,-1.92966607280848));
#9460=CARTESIAN_POINT('',(13.3,-21.9999999999999,-5.92966607280848));
#9461=CARTESIAN_POINT('Origin',(13.3,-21.9999999999999,-6.22966607280848));
#9462=CARTESIAN_POINT('',(13.3,-25.9999999999999,-1.92966607280848));
#9463=CARTESIAN_POINT('Origin',(13.3,-21.9999999999999,-1.92966607280848));
#9464=CARTESIAN_POINT('Origin',(13.3,-21.9999999999999,-1.92966607280848));
#9465=CARTESIAN_POINT('Origin',(13.,-21.9999999999999,-1.92966607280848));
#9466=CARTESIAN_POINT('',(13.,-21.9999999999999,2.77033392719152));
#9467=CARTESIAN_POINT('Origin',(13.,-21.9999999999999,-1.92966607280848));
#9468=CARTESIAN_POINT('Origin',(29.,-21.9999999999999,-1.92966607280848));
#9469=CARTESIAN_POINT('',(28.7,-25.9999999999999,-1.92966607280848));
#9470=CARTESIAN_POINT('',(29.,-25.9999999999999,-1.92966607280848));
#9471=CARTESIAN_POINT('',(28.7,-21.9999999999999,2.07033392719152));
#9472=CARTESIAN_POINT('Origin',(28.7,-21.9999999999999,-1.92966607280848));
#9473=CARTESIAN_POINT('Origin',(28.7,-21.9999999999999,-1.92966607280848));
#9474=CARTESIAN_POINT('Origin',(13.3,-21.9999999999999,-1.92966607280848));
#9475=CARTESIAN_POINT('',(13.3,-21.9999999999999,3.07033392719152));
#9476=CARTESIAN_POINT('Origin',(13.3,-21.9999999999999,2.77033392719152));
#9477=CARTESIAN_POINT('',(13.3,-26.9999999999999,-1.92966607280848));
#9478=CARTESIAN_POINT('Origin',(13.3,-21.9999999999999,-1.92966607280848));
#9479=CARTESIAN_POINT('Origin',(13.3,-21.9999999999999,-1.92966607280848));
#9480=CARTESIAN_POINT('Origin',(29.,-21.9999999999999,-1.92966607280848));
#9481=CARTESIAN_POINT('',(28.7,-26.9999999999999,-1.92966607280848));
#9482=CARTESIAN_POINT('',(29.,-26.9999999999999,-1.92966607280848));
#9483=CARTESIAN_POINT('',(28.7,-21.9999999999999,-6.92966607280848));
#9484=CARTESIAN_POINT('Origin',(28.7,-21.9999999999999,-1.92966607280848));
#9485=CARTESIAN_POINT('Origin',(28.7,-21.9999999999999,-1.92966607280848));
#9486=CARTESIAN_POINT('Origin',(28.7,-21.9999999999999,-1.92966607280848));
#9487=CARTESIAN_POINT('',(29.,-21.9999999999999,2.37033392719152));
#9488=CARTESIAN_POINT('Origin',(29.,-21.9999999999999,-1.92966607280848));
#9489=CARTESIAN_POINT('Origin',(28.7,-21.9999999999999,2.37033392719152));
#9490=CARTESIAN_POINT('Origin',(29.,-21.9999999999999,-1.92966607280848));
#9491=CARTESIAN_POINT('',(29.,-21.9999999999999,-6.62966607280848));
#9492=CARTESIAN_POINT('Origin',(29.,-21.9999999999999,-1.92966607280848));
#9493=CARTESIAN_POINT('Origin',(28.7,-21.9999999999999,-1.92966607280848));
#9494=CARTESIAN_POINT('Origin',(28.7,-21.9999999999999,-6.62966607280848));
#10619=UNCERTAINTY_MEASURE_WITH_UNIT(LENGTH_MEASURE(0.01),#10640,
'DISTANCE_ACCURACY_VALUE',
'Maximum model space distance between geometric entities at asserted c
onnectivities');
#10627=UNCERTAINTY_MEASURE_WITH_UNIT(LENGTH_MEASURE(0.01),#10640,
'DISTANCE_ACCURACY_VALUE',
'Maximum model space distance between geometric entities at asserted c
onnectivities');
#10631=(
GEOMETRIC_REPRESENTATION_CONTEXT(3)
GLOBAL_UNCERTAINTY_ASSIGNED_CONTEXT((#10619))
GLOBAL_UNIT_ASSIGNED_CONTEXT((#10640,#10642,#10643))
REPRESENTATION_CONTEXT('','3D')
);
#10639=(
GEOMETRIC_REPRESENTATION_CONTEXT(3)
GLOBAL_UNCERTAINTY_ASSIGNED_CONTEXT((#10627))
GLOBAL_UNIT_ASSIGNED_CONTEXT((#10640,#10642,#10643))
REPRESENTATION_CONTEXT('','3D')
);
#10640=(
LENGTH_UNIT()
NAMED_UNIT(*)
SI_UNIT(.MILLI.,.METRE.)
);
#10642=(
NAMED_UNIT(*)
PLANE_ANGLE_UNIT()
SI_UNIT($,.RADIAN.)
);
#10643=(
NAMED_UNIT(*)
SI_UNIT($,.STERADIAN.)
SOLID_ANGLE_UNIT()
);
#10647=SHAPE_DEFINITION_REPRESENTATION(#10658,#10679);
#10658=PRODUCT_DEFINITION_SHAPE('',$,#10691);
#10679=SHAPE_REPRESENTATION('',(#6199),#10631);
#10687=PRODUCT_DEFINITION_CONTEXT('part definition',#10722,'design');
#10691=PRODUCT_DEFINITION('Bearing_04','Bearing_04',#10702,#10687);
#10702=PRODUCT_DEFINITION_FORMATION('',$,#10727);
#10722=APPLICATION_CONTEXT(
'Core Data for Automotive Mechanical Design Process');
#10723=PRODUCT_CONTEXT('part definition',#10722,'mechanical');
#10727=PRODUCT('Bearing_04','Bearing_04',$,(#10723));
#10784=COLOUR_RGB('Grey',0.48,0.52,0.57);
#10785=FILL_AREA_STYLE_COLOUR('',#10784);
#10786=FILL_AREA_STYLE('',(#10785));
#10787=SURFACE_STYLE_FILL_AREA(#10786);
#10788=SURFACE_SIDE_STYLE('',(#10787));
#10789=SURFACE_STYLE_USAGE(.BOTH.,#10788);
#10790=PRESENTATION_STYLE_ASSIGNMENT((#10789));
ENDSEC;
END-ISO-10303-21;
